ISO-10303-21;
HEADER;
/* Generated by software containing ST-Developer
 * from STEP Tools, Inc. (www.steptools.com) 
 */

FILE_DESCRIPTION(
/* description */ ('PAT-122'),
/* implementation_level */ '2;1');

FILE_NAME(
/* name */ 'Flat Washer - M4.step',
/* time_stamp */ '2026-10-29T20:20:12-07:00',
/* author */ (''),
/* organization */ (''),
/* preprocessor_version */ 'ST-DEVELOPER v20.2',
/* originating_system */ 'Autodesk Translation Framework v15.17.0.0',
/* authorisation */ '');

FILE_SCHEMA (('AUTOMOTIVE_DESIGN { 1 0 10303 214 3 1 1 }'));
ENDSEC;

DATA;
#10=MECHANICAL_DESIGN_GEOMETRIC_PRESENTATION_REPRESENTATION('',(#511),#10019);
#412=CONICAL_SURFACE('',#6293,0.225,0.785398163397448);
#467=SHAPE_REPRESENTATION_RELATIONSHIP('SRR','None',#10188,#489);
#489=ADVANCED_BREP_SHAPE_REPRESENTATION('',(#530),#10017);
#511=STYLED_ITEM('',(#10355),#530);
#530=MANIFOLD_SOLID_BREP('Body1',#5636);
#606=FACE_BOUND('',#1465,.T.);
#607=FACE_BOUND('',#1468,.T.);
#812=PLANE('',#6298);
#813=PLANE('',#6302);
#1095=FACE_OUTER_BOUND('',#1462,.T.);
#1096=FACE_OUTER_BOUND('',#1463,.T.);
#1097=FACE_OUTER_BOUND('',#1464,.T.);
#1098=FACE_OUTER_BOUND('',#1466,.T.);
#1099=FACE_OUTER_BOUND('',#1467,.T.);
#1462=EDGE_LOOP('',(#5181,#5182,#5183,#5184));
#1463=EDGE_LOOP('',(#5185,#5186,#5187,#5188));
#1464=EDGE_LOOP('',(#5189));
#1465=EDGE_LOOP('',(#5190));
#1466=EDGE_LOOP('',(#5191,#5192,#5193,#5194));
#1467=EDGE_LOOP('',(#5195));
#1468=EDGE_LOOP('',(#5196));
#2004=LINE('',#9791,#2548);
#2005=LINE('',#9795,#2549);
#2006=LINE('',#9802,#2550);
#2548=VECTOR('',#7769,0.225);
#2549=VECTOR('',#7774,0.215);
#2550=VECTOR('',#7783,0.45);
#2692=CIRCLE('',#6294,0.235);
#2693=CIRCLE('',#6295,0.215);
#2694=CIRCLE('',#6297,0.215);
#2695=CIRCLE('',#6299,0.45);
#2696=CIRCLE('',#6301,0.45);
#3142=VERTEX_POINT('',#9788);
#3143=VERTEX_POINT('',#9790);
#3144=VERTEX_POINT('',#9794);
#3145=VERTEX_POINT('',#9798);
#3146=VERTEX_POINT('',#9801);
#3825=EDGE_CURVE('',#3142,#3142,#2692,.T.);
#3826=EDGE_CURVE('',#3142,#3143,#2004,.T.);
#3827=EDGE_CURVE('',#3143,#3143,#2693,.T.);
#3828=EDGE_CURVE('',#3143,#3144,#2005,.T.);
#3829=EDGE_CURVE('',#3144,#3144,#2694,.T.);
#3830=EDGE_CURVE('',#3145,#3145,#2695,.T.);
#3831=EDGE_CURVE('',#3145,#3146,#2006,.T.);
#3832=EDGE_CURVE('',#3146,#3146,#2696,.T.);
#5181=ORIENTED_EDGE('',*,*,#3825,.T.);
#5182=ORIENTED_EDGE('',*,*,#3826,.T.);
#5183=ORIENTED_EDGE('',*,*,#3827,.T.);
#5184=ORIENTED_EDGE('',*,*,#3826,.F.);
#5185=ORIENTED_EDGE('',*,*,#3827,.F.);
#5186=ORIENTED_EDGE('',*,*,#3828,.T.);
#5187=ORIENTED_EDGE('',*,*,#3829,.T.);
#5188=ORIENTED_EDGE('',*,*,#3828,.F.);
#5189=ORIENTED_EDGE('',*,*,#3830,.T.);
#5190=ORIENTED_EDGE('',*,*,#3825,.F.);
#5191=ORIENTED_EDGE('',*,*,#3830,.F.);
#5192=ORIENTED_EDGE('',*,*,#3831,.T.);
#5193=ORIENTED_EDGE('',*,*,#3832,.T.);
#5194=ORIENTED_EDGE('',*,*,#3831,.F.);
#5195=ORIENTED_EDGE('',*,*,#3832,.F.);
#5196=ORIENTED_EDGE('',*,*,#3829,.F.);
#5317=CYLINDRICAL_SURFACE('',#6296,0.215);
#5318=CYLINDRICAL_SURFACE('',#6300,0.45);
#5591=ADVANCED_FACE('',(#1095),#412,.F.);
#5592=ADVANCED_FACE('',(#1096),#5317,.F.);
#5593=ADVANCED_FACE('',(#1097,#606),#812,.T.);
#5594=ADVANCED_FACE('',(#1098),#5318,.T.);
#5595=ADVANCED_FACE('',(#1099,#607),#813,.F.);
#5636=CLOSED_SHELL('',(#5591,#5592,#5593,#5594,#5595));
#6292=AXIS2_PLACEMENT_3D('',#9786,#7763,#7764);
#6293=AXIS2_PLACEMENT_3D('',#9787,#7765,#7766);
#6294=AXIS2_PLACEMENT_3D('',#9789,#7767,#7768);
#6295=AXIS2_PLACEMENT_3D('',#9792,#7770,#7771);
#6296=AXIS2_PLACEMENT_3D('',#9793,#7772,#7773);
#6297=AXIS2_PLACEMENT_3D('',#9796,#7775,#7776);
#6298=AXIS2_PLACEMENT_3D('',#9797,#7777,#7778);
#6299=AXIS2_PLACEMENT_3D('',#9799,#7779,#7780);
#6300=AXIS2_PLACEMENT_3D('',#9800,#7781,#7782);
#6301=AXIS2_PLACEMENT_3D('',#9803,#7784,#7785);
#6302=AXIS2_PLACEMENT_3D('',#9804,#7786,#7787);
#7763=DIRECTION('axis',(0.,0.,1.));
#7764=DIRECTION('refdir',(1.,0.,0.));
#7765=DIRECTION('center_axis',(0.,1.,0.));
#7766=DIRECTION('ref_axis',(1.,0.,0.));
#7767=DIRECTION('center_axis',(0.,1.,0.));
#7768=DIRECTION('ref_axis',(1.,0.,0.));
#7769=DIRECTION('',(0.707106781186547,-0.707106781186548,-8.65956056235493E-17));
#7770=DIRECTION('center_axis',(0.,-1.,0.));
#7771=DIRECTION('ref_axis',(1.,0.,0.));
#7772=DIRECTION('center_axis',(0.,1.,0.));
#7773=DIRECTION('ref_axis',(1.,0.,0.));
#7774=DIRECTION('',(0.,-1.,0.));
#7775=DIRECTION('center_axis',(0.,-1.,0.));
#7776=DIRECTION('ref_axis',(1.,0.,0.));
#7777=DIRECTION('center_axis',(0.,1.,0.));
#7778=DIRECTION('ref_axis',(1.,0.,0.));
#7779=DIRECTION('center_axis',(0.,1.,0.));
#7780=DIRECTION('ref_axis',(1.,0.,0.));
#7781=DIRECTION('center_axis',(0.,1.,0.));
#7782=DIRECTION('ref_axis',(1.,0.,0.));
#7783=DIRECTION('',(0.,-1.,0.));
#7784=DIRECTION('center_axis',(0.,1.,0.));
#7785=DIRECTION('ref_axis',(1.,0.,0.));
#7786=DIRECTION('center_axis',(0.,1.,0.));
#7787=DIRECTION('ref_axis',(1.,0.,0.));
#9786=CARTESIAN_POINT('',(0.,0.,0.));
#9787=CARTESIAN_POINT('Origin',(0.,0.07,0.));
#9788=CARTESIAN_POINT('',(-0.235,0.08,2.87791997799628E-17));
#9789=CARTESIAN_POINT('Origin',(0.,0.08,0.));
#9790=CARTESIAN_POINT('',(-0.215,0.06,-2.63299061816681E-17));
#9791=CARTESIAN_POINT('',(-0.225,0.07,2.75545529808154E-17));
#9792=CARTESIAN_POINT('Origin',(0.,0.06,0.));
#9793=CARTESIAN_POINT('Origin',(0.,0.,0.));
#9794=CARTESIAN_POINT('',(-0.215,0.,2.63299061816681E-17));
#9795=CARTESIAN_POINT('',(-0.215,0.,2.63299061816681E-17));
#9796=CARTESIAN_POINT('Origin',(0.,0.,0.));
#9797=CARTESIAN_POINT('Origin',(0.,0.08,0.));
#9798=CARTESIAN_POINT('',(-0.45,0.08,5.51091059616309E-17));
#9799=CARTESIAN_POINT('Origin',(0.,0.08,0.));
#9800=CARTESIAN_POINT('Origin',(0.,0.,0.));
#9801=CARTESIAN_POINT('',(-0.45,0.,5.51091059616309E-17));
#9802=CARTESIAN_POINT('',(-0.45,0.,5.51091059616309E-17));
#9803=CARTESIAN_POINT('Origin',(0.,0.,0.));
#9804=CARTESIAN_POINT('Origin',(0.,0.,0.));
#9993=UNCERTAINTY_MEASURE_WITH_UNIT(LENGTH_MEASURE(0.001),#10020,
'DISTANCE_ACCURACY_VALUE',
'Maximum model space distance between geometric entities at asserted c
onnectivities');
#9995=UNCERTAINTY_MEASURE_WITH_UNIT(LENGTH_MEASURE(0.001),#10020,
'DISTANCE_ACCURACY_VALUE',
'Maximum model space distance between geometric entities at asserted c
onnectivities');
#10017=(
GEOMETRIC_REPRESENTATION_CONTEXT(3)
GLOBAL_UNCERTAINTY_ASSIGNED_CONTEXT((#9993))
GLOBAL_UNIT_ASSIGNED_CONTEXT((#10020,#10022,#10023))
REPRESENTATION_CONTEXT('','3D')
);
#10019=(
GEOMETRIC_REPRESENTATION_CONTEXT(3)
GLOBAL_UNCERTAINTY_ASSIGNED_CONTEXT((#9995))
GLOBAL_UNIT_ASSIGNED_CONTEXT((#10020,#10022,#10023))
REPRESENTATION_CONTEXT('','3D')
);
#10020=(
LENGTH_UNIT()
NAMED_UNIT(*)
SI_UNIT(.CENTI.,.METRE.)
);
#10022=(
NAMED_UNIT(*)
PLANE_ANGLE_UNIT()
SI_UNIT($,.RADIAN.)
);
#10023=(
NAMED_UNIT(*)
SI_UNIT($,.STERADIAN.)
SOLID_ANGLE_UNIT()
);
#10045=SHAPE_DEFINITION_REPRESENTATION(#10068,#10188);
#10068=PRODUCT_DEFINITION_SHAPE('',$,#10212);
#10188=SHAPE_REPRESENTATION('',(#6292),#10017);
#10190=PRODUCT_DEFINITION_CONTEXT('part definition',#10261,'design');
#10212=PRODUCT_DEFINITION('Flat Washer - M4',
'Flat Washer - M4',#10235,#10190);
#10235=PRODUCT_DEFINITION_FORMATION('',$,#10284);
#10261=APPLICATION_CONTEXT(
'Core Data for Automotive Mechanical Design Process');
#10262=PRODUCT_CONTEXT('part definition',#10261,'mechanical');
#10284=PRODUCT('Flat Washer - M4','Flat Washer - M4',
'Flat Washer - M4',(#10262));
#10349=COLOUR_RGB('Black',0.12,0.14,0.17);
#10350=FILL_AREA_STYLE_COLOUR('',#10349);
#10351=FILL_AREA_STYLE('',(#10350));
#10352=SURFACE_STYLE_FILL_AREA(#10351);
#10353=SURFACE_SIDE_STYLE('',(#10352));
#10354=SURFACE_STYLE_USAGE(.BOTH.,#10353);
#10355=PRESENTATION_STYLE_ASSIGNMENT((#10354));
ENDSEC;
END-ISO-10303-21;
